ISO-10303-21;
HEADER;
/* Generated by software containing ST-Developer
 * from STEP Tools, Inc. (www.steptools.com) 
 */

FILE_DESCRIPTION(
/* description */ ('Timing belt drive module 2 mm Pitch Timing 20T-40T'),

/* implementation_level */ '2;1');

FILE_NAME(
/* name */ 'Output M3 set screw (1).step',
/* time_stamp */ '2026-10-28T03:25:12-07:00',
/* author */ (''),
/* organization */ (''),
/* preprocessor_version */ 'ST-DEVELOPER v20.2',
/* originating_system */ 'Autodesk Translation Framework v15.17.0.0',
/* authorisation */ '');

FILE_SCHEMA (('AUTOMOTIVE_DESIGN { 1 0 10303 214 3 1 1 }'));
ENDSEC;

DATA;
#10=MECHANICAL_DESIGN_GEOMETRIC_PRESENTATION_REPRESENTATION('',(#578),#17830);
#477=SHAPE_REPRESENTATION_RELATIONSHIP('SRR','None',#18051,#520);
#520=ADVANCED_BREP_SHAPE_REPRESENTATION('',(#634),#17826);
#578=STYLED_ITEM('',(#18324),#634);
#634=MANIFOLD_SOLID_BREP('Body1',#9037);
#942=PLANE('',#10447);
#943=PLANE('',#10448);
#1366=FACE_OUTER_BOUND('',#2009,.T.);
#1367=FACE_OUTER_BOUND('',#2010,.T.);
#1368=FACE_OUTER_BOUND('',#2011,.T.);
#2009=EDGE_LOOP('',(#7539,#7540,#7541,#7542));
#2010=EDGE_LOOP('',(#7543));
#2011=EDGE_LOOP('',(#7544));
#2608=CIRCLE('',#10445,0.15);
#2609=CIRCLE('',#10446,0.15);
#3151=LINE('',#16737,#3629);
#3629=VECTOR('',#13030,0.15);
#4353=VERTEX_POINT('',#16734);
#4354=VERTEX_POINT('',#16736);
#5452=EDGE_CURVE('',#4353,#4353,#2608,.T.);
#5453=EDGE_CURVE('',#4353,#4354,#3151,.T.);
#5454=EDGE_CURVE('',#4354,#4354,#2609,.T.);
#7539=ORIENTED_EDGE('',*,*,#5452,.F.);
#7540=ORIENTED_EDGE('',*,*,#5453,.T.);
#7541=ORIENTED_EDGE('',*,*,#5454,.T.);
#7542=ORIENTED_EDGE('',*,*,#5453,.F.);
#7543=ORIENTED_EDGE('',*,*,#5452,.T.);
#7544=ORIENTED_EDGE('',*,*,#5454,.F.);
#8367=CYLINDRICAL_SURFACE('',#10444,0.15);
#8864=ADVANCED_FACE('',(#1366),#8367,.T.);
#8865=ADVANCED_FACE('',(#1367),#942,.T.);
#8866=ADVANCED_FACE('',(#1368),#943,.F.);
#9037=CLOSED_SHELL('',(#8864,#8865,#8866));
#10443=AXIS2_PLACEMENT_3D('',#16732,#13024,#13025);
#10444=AXIS2_PLACEMENT_3D('',#16733,#13026,#13027);
#10445=AXIS2_PLACEMENT_3D('',#16735,#13028,#13029);
#10446=AXIS2_PLACEMENT_3D('',#16738,#13031,#13032);
#10447=AXIS2_PLACEMENT_3D('',#16739,#13033,#13034);
#10448=AXIS2_PLACEMENT_3D('',#16740,#13035,#13036);
#13024=DIRECTION('axis',(0.,0.,1.));
#13025=DIRECTION('refdir',(1.,0.,0.));
#13026=DIRECTION('center_axis',(0.,0.,1.));
#13027=DIRECTION('ref_axis',(1.,0.,0.));
#13028=DIRECTION('center_axis',(0.,0.,1.));
#13029=DIRECTION('ref_axis',(1.,0.,0.));
#13030=DIRECTION('',(0.,0.,-1.));
#13031=DIRECTION('center_axis',(0.,0.,1.));
#13032=DIRECTION('ref_axis',(1.,0.,0.));
#13033=DIRECTION('center_axis',(0.,0.,1.));
#13034=DIRECTION('ref_axis',(1.,0.,0.));
#13035=DIRECTION('center_axis',(0.,0.,1.));
#13036=DIRECTION('ref_axis',(1.,0.,0.));
#16732=CARTESIAN_POINT('',(0.,0.,0.));
#16733=CARTESIAN_POINT('Origin',(6.97091003018116,-4.,7.6));
#16734=CARTESIAN_POINT('',(6.82091003018116,-4.,8.));
#16735=CARTESIAN_POINT('Origin',(6.97091003018116,-4.,8.));
#16736=CARTESIAN_POINT('',(6.82091003018116,-4.,7.6));
#16737=CARTESIAN_POINT('',(6.82091003018116,-4.,7.6));
#16738=CARTESIAN_POINT('Origin',(6.97091003018116,-4.,7.6));
#16739=CARTESIAN_POINT('Origin',(6.97091003018116,-4.,8.));
#16740=CARTESIAN_POINT('Origin',(6.97091003018116,-4.,7.6));
#17776=UNCERTAINTY_MEASURE_WITH_UNIT(LENGTH_MEASURE(0.001),#17831,
'DISTANCE_ACCURACY_VALUE',
'Maximum model space distance between geometric entities at asserted c
onnectivities');
#17780=UNCERTAINTY_MEASURE_WITH_UNIT(LENGTH_MEASURE(0.001),#17831,
'DISTANCE_ACCURACY_VALUE',
'Maximum model space distance between geometric entities at asserted c
onnectivities');
#17826=(
GEOMETRIC_REPRESENTATION_CONTEXT(3)
GLOBAL_UNCERTAINTY_ASSIGNED_CONTEXT((#17776))
GLOBAL_UNIT_ASSIGNED_CONTEXT((#17831,#17833,#17834))
REPRESENTATION_CONTEXT('','3D')
);
#17830=(
GEOMETRIC_REPRESENTATION_CONTEXT(3)
GLOBAL_UNCERTAINTY_ASSIGNED_CONTEXT((#17780))
GLOBAL_UNIT_ASSIGNED_CONTEXT((#17831,#17833,#17834))
REPRESENTATION_CONTEXT('','3D')
);
#17831=(
LENGTH_UNIT()
NAMED_UNIT(*)
SI_UNIT(.CENTI.,.METRE.)
);
#17833=(
NAMED_UNIT(*)
PLANE_ANGLE_UNIT()
SI_UNIT($,.RADIAN.)
);
#17834=(
NAMED_UNIT(*)
SI_UNIT($,.STERADIAN.)
SOLID_ANGLE_UNIT()
);
#17880=SHAPE_DEFINITION_REPRESENTATION(#17939,#18051);
#17939=PRODUCT_DEFINITION_SHAPE('',$,#18101);
#18051=SHAPE_REPRESENTATION('',(#10443),#17826);
#18055=PRODUCT_DEFINITION_CONTEXT('part definition',#18204,'design');
#18101=PRODUCT_DEFINITION('Output M3 set screw (1)',
'Output M3 set screw (1)',#18150,#18055);
#18150=PRODUCT_DEFINITION_FORMATION('',$,#18251);
#18204=APPLICATION_CONTEXT(
'Core Data for Automotive Mechanical Design Process');
#18205=PRODUCT_CONTEXT('part definition',#18204,'mechanical');
#18251=PRODUCT('Output M3 set screw (1)','Output M3 set screw (1)',
'Output M3 set screw (1)',(#18205));
#18318=COLOUR_RGB('Black',0.12,0.14,0.17);
#18319=FILL_AREA_STYLE_COLOUR('',#18318);
#18320=FILL_AREA_STYLE('',(#18319));
#18321=SURFACE_STYLE_FILL_AREA(#18320);
#18322=SURFACE_SIDE_STYLE('',(#18321));
#18323=SURFACE_STYLE_USAGE(.BOTH.,#18322);
#18324=PRESENTATION_STYLE_ASSIGNMENT((#18323));
ENDSEC;
END-ISO-10303-21;
